ISO-10303-21;
HEADER;
/* Generated by software containing ST-Developer
 * from STEP Tools, Inc. (www.steptools.com) 
 */

FILE_DESCRIPTION(
/* description */ ('Chute with adjustable gate'),
/* implementation_level */ '2;1');

FILE_NAME(
/* name */ 'M5x30 frame screw.step',
/* time_stamp */ '2026-10-27T10:52:28-07:00',
/* author */ (''),
/* organization */ (''),
/* preprocessor_version */ 'ST-DEVELOPER v20.2',
/* originating_system */ 'Autodesk Translation Framework v15.17.0.0',
/* authorisation */ '');

FILE_SCHEMA (('AUTOMOTIVE_DESIGN { 1 0 10303 214 3 1 1 }'));
ENDSEC;

DATA;
#10=MECHANICAL_DESIGN_GEOMETRIC_PRESENTATION_REPRESENTATION('',(#438),#13094);
#328=ORIENTED_CLOSED_SHELL('',*,#7622,.F.);
#336=CONICAL_SURFACE('',#8439,0.4,0.785398163397448);
#337=CONICAL_SURFACE('',#8443,0.41,0.785398163397448);
#338=CONICAL_SURFACE('',#8447,0.26,0.463647609000806);
#347=BREP_WITH_VOIDS('Body1',#7623,(#328));
#374=SHAPE_REPRESENTATION_RELATIONSHIP('SRR','None',#13275,#406);
#406=ADVANCED_BREP_SHAPE_REPRESENTATION('',(#347),#13084);
#438=STYLED_ITEM('',(#13502),#347);
#568=FACE_BOUND('',#1725,.T.);
#569=FACE_BOUND('',#1733,.T.);
#824=PLANE('',#8423);
#825=PLANE('',#8424);
#826=PLANE('',#8425);
#827=PLANE('',#8426);
#828=PLANE('',#8427);
#829=PLANE('',#8428);
#830=PLANE('',#8429);
#831=PLANE('',#8430);
#832=PLANE('',#8431);
#833=PLANE('',#8436);
#834=PLANE('',#8437);
#835=PLANE('',#8445);
#1207=FACE_OUTER_BOUND('',#1716,.T.);
#1208=FACE_OUTER_BOUND('',#1717,.T.);
#1209=FACE_OUTER_BOUND('',#1718,.T.);
#1210=FACE_OUTER_BOUND('',#1719,.T.);
#1211=FACE_OUTER_BOUND('',#1720,.T.);
#1212=FACE_OUTER_BOUND('',#1721,.T.);
#1213=FACE_OUTER_BOUND('',#1722,.T.);
#1214=FACE_OUTER_BOUND('',#1723,.T.);
#1215=FACE_OUTER_BOUND('',#1724,.T.);
#1216=FACE_OUTER_BOUND('',#1726,.T.);
#1217=FACE_OUTER_BOUND('',#1727,.T.);
#1218=FACE_OUTER_BOUND('',#1728,.T.);
#1219=FACE_OUTER_BOUND('',#1729,.T.);
#1220=FACE_OUTER_BOUND('',#1730,.T.);
#1221=FACE_OUTER_BOUND('',#1731,.T.);
#1222=FACE_OUTER_BOUND('',#1732,.T.);
#1223=FACE_OUTER_BOUND('',#1734,.T.);
#1224=FACE_OUTER_BOUND('',#1735,.T.);
#1716=EDGE_LOOP('',(#6550,#6551,#6552,#6553));
#1717=EDGE_LOOP('',(#6554,#6555,#6556,#6557));
#1718=EDGE_LOOP('',(#6558,#6559,#6560,#6561));
#1719=EDGE_LOOP('',(#6562,#6563,#6564,#6565));
#1720=EDGE_LOOP('',(#6566,#6567,#6568,#6569));
#1721=EDGE_LOOP('',(#6570,#6571,#6572,#6573));
#1722=EDGE_LOOP('',(#6574,#6575,#6576,#6577,#6578,#6579));
#1723=EDGE_LOOP('',(#6580,#6581,#6582,#6583,#6584,#6585));
#1724=EDGE_LOOP('',(#6586));
#1725=EDGE_LOOP('',(#6587));
#1726=EDGE_LOOP('',(#6588,#6589,#6590,#6591));
#1727=EDGE_LOOP('',(#6592));
#1728=EDGE_LOOP('',(#6593));
#1729=EDGE_LOOP('',(#6594,#6595,#6596,#6597));
#1730=EDGE_LOOP('',(#6598,#6599,#6600,#6601));
#1731=EDGE_LOOP('',(#6602,#6603,#6604,#6605));
#1732=EDGE_LOOP('',(#6606));
#1733=EDGE_LOOP('',(#6607));
#1734=EDGE_LOOP('',(#6608,#6609,#6610,#6611));
#1735=EDGE_LOOP('',(#6612,#6613,#6614,#6615));
#2425=LINE('',#12357,#3202);
#2426=LINE('',#12359,#3203);
#2427=LINE('',#12361,#3204);
#2428=LINE('',#12362,#3205);
#2429=LINE('',#12365,#3206);
#2430=LINE('',#12367,#3207);
#2431=LINE('',#12368,#3208);
#2432=LINE('',#12371,#3209);
#2433=LINE('',#12373,#3210);
#2434=LINE('',#12374,#3211);
#2435=LINE('',#12377,#3212);
#2436=LINE('',#12379,#3213);
#2437=LINE('',#12380,#3214);
#2438=LINE('',#12383,#3215);
#2439=LINE('',#12385,#3216);
#2440=LINE('',#12386,#3217);
#2441=LINE('',#12388,#3218);
#2442=LINE('',#12389,#3219);
#2443=LINE('',#12399,#3220);
#2444=LINE('',#12408,#3221);
#2445=LINE('',#12412,#3222);
#2446=LINE('',#12416,#3223);
#2447=LINE('',#12423,#3224);
#2448=LINE('',#12425,#3225);
#3202=VECTOR('',#10139,1.);
#3203=VECTOR('',#10140,1.);
#3204=VECTOR('',#10141,1.);
#3205=VECTOR('',#10142,1.);
#3206=VECTOR('',#10145,1.);
#3207=VECTOR('',#10146,1.);
#3208=VECTOR('',#10147,1.);
#3209=VECTOR('',#10150,1.);
#3210=VECTOR('',#10151,1.);
#3211=VECTOR('',#10152,1.);
#3212=VECTOR('',#10155,1.);
#3213=VECTOR('',#10156,1.);
#3214=VECTOR('',#10157,1.);
#3215=VECTOR('',#10160,1.);
#3216=VECTOR('',#10161,1.);
#3217=VECTOR('',#10162,1.);
#3218=VECTOR('',#10165,1.);
#3219=VECTOR('',#10166,1.);
#3220=VECTOR('',#10179,0.25);
#3221=VECTOR('',#10192,0.4);
#3222=VECTOR('',#10197,0.425);
#3223=VECTOR('',#10202,0.41);
#3224=VECTOR('',#10211,0.26);
#3225=VECTOR('',#10214,0.25);
#3529=CIRCLE('',#8432,0.25);
#3530=CIRCLE('',#8433,0.24505);
#3531=CIRCLE('',#8435,0.25);
#3532=CIRCLE('',#8438,0.375);
#3533=CIRCLE('',#8440,0.425);
#3534=CIRCLE('',#8442,0.425);
#3535=CIRCLE('',#8444,0.395);
#3536=CIRCLE('',#8446,0.27);
#3537=CIRCLE('',#8448,0.24505);
#4046=VERTEX_POINT('',#12355);
#4047=VERTEX_POINT('',#12356);
#4048=VERTEX_POINT('',#12358);
#4049=VERTEX_POINT('',#12360);
#4050=VERTEX_POINT('',#12364);
#4051=VERTEX_POINT('',#12366);
#4052=VERTEX_POINT('',#12370);
#4053=VERTEX_POINT('',#12372);
#4054=VERTEX_POINT('',#12376);
#4055=VERTEX_POINT('',#12378);
#4056=VERTEX_POINT('',#12382);
#4057=VERTEX_POINT('',#12384);
#4058=VERTEX_POINT('',#12393);
#4059=VERTEX_POINT('',#12395);
#4060=VERTEX_POINT('',#12398);
#4061=VERTEX_POINT('',#12403);
#4062=VERTEX_POINT('',#12406);
#4063=VERTEX_POINT('',#12410);
#4064=VERTEX_POINT('',#12414);
#4065=VERTEX_POINT('',#12418);
#4066=VERTEX_POINT('',#12421);
#4908=EDGE_CURVE('',#4046,#4047,#2425,.T.);
#4909=EDGE_CURVE('',#4047,#4048,#2426,.T.);
#4910=EDGE_CURVE('',#4048,#4049,#2427,.T.);
#4911=EDGE_CURVE('',#4046,#4049,#2428,.T.);
#4912=EDGE_CURVE('',#4047,#4050,#2429,.T.);
#4913=EDGE_CURVE('',#4050,#4051,#2430,.T.);
#4914=EDGE_CURVE('',#4051,#4048,#2431,.T.);
#4915=EDGE_CURVE('',#4050,#4052,#2432,.T.);
#4916=EDGE_CURVE('',#4052,#4053,#2433,.T.);
#4917=EDGE_CURVE('',#4053,#4051,#2434,.T.);
#4918=EDGE_CURVE('',#4052,#4054,#2435,.T.);
#4919=EDGE_CURVE('',#4054,#4055,#2436,.T.);
#4920=EDGE_CURVE('',#4055,#4053,#2437,.T.);
#4921=EDGE_CURVE('',#4054,#4056,#2438,.T.);
#4922=EDGE_CURVE('',#4056,#4057,#2439,.T.);
#4923=EDGE_CURVE('',#4057,#4055,#2440,.T.);
#4924=EDGE_CURVE('',#4056,#4046,#2441,.T.);
#4925=EDGE_CURVE('',#4049,#4057,#2442,.T.);
#4926=EDGE_CURVE('',#4058,#4058,#3529,.T.);
#4927=EDGE_CURVE('',#4059,#4059,#3530,.T.);
#4928=EDGE_CURVE('',#4058,#4060,#2443,.T.);
#4929=EDGE_CURVE('',#4060,#4060,#3531,.T.);
#4930=EDGE_CURVE('',#4061,#4061,#3532,.T.);
#4931=EDGE_CURVE('',#4062,#4062,#3533,.T.);
#4932=EDGE_CURVE('',#4062,#4061,#2444,.T.);
#4933=EDGE_CURVE('',#4063,#4063,#3534,.T.);
#4934=EDGE_CURVE('',#4063,#4062,#2445,.T.);
#4935=EDGE_CURVE('',#4064,#4064,#3535,.T.);
#4936=EDGE_CURVE('',#4064,#4063,#2446,.T.);
#4937=EDGE_CURVE('',#4065,#4065,#3536,.T.);
#4938=EDGE_CURVE('',#4066,#4066,#3537,.F.);
#4939=EDGE_CURVE('',#4066,#4065,#2447,.T.);
#4940=EDGE_CURVE('',#4059,#4066,#2448,.T.);
#6550=ORIENTED_EDGE('',*,*,#4908,.T.);
#6551=ORIENTED_EDGE('',*,*,#4909,.T.);
#6552=ORIENTED_EDGE('',*,*,#4910,.T.);
#6553=ORIENTED_EDGE('',*,*,#4911,.F.);
#6554=ORIENTED_EDGE('',*,*,#4912,.T.);
#6555=ORIENTED_EDGE('',*,*,#4913,.T.);
#6556=ORIENTED_EDGE('',*,*,#4914,.T.);
#6557=ORIENTED_EDGE('',*,*,#4909,.F.);
#6558=ORIENTED_EDGE('',*,*,#4915,.T.);
#6559=ORIENTED_EDGE('',*,*,#4916,.T.);
#6560=ORIENTED_EDGE('',*,*,#4917,.T.);
#6561=ORIENTED_EDGE('',*,*,#4913,.F.);
#6562=ORIENTED_EDGE('',*,*,#4918,.T.);
#6563=ORIENTED_EDGE('',*,*,#4919,.T.);
#6564=ORIENTED_EDGE('',*,*,#4920,.T.);
#6565=ORIENTED_EDGE('',*,*,#4916,.F.);
#6566=ORIENTED_EDGE('',*,*,#4921,.T.);
#6567=ORIENTED_EDGE('',*,*,#4922,.T.);
#6568=ORIENTED_EDGE('',*,*,#4923,.T.);
#6569=ORIENTED_EDGE('',*,*,#4919,.F.);
#6570=ORIENTED_EDGE('',*,*,#4924,.T.);
#6571=ORIENTED_EDGE('',*,*,#4911,.T.);
#6572=ORIENTED_EDGE('',*,*,#4925,.T.);
#6573=ORIENTED_EDGE('',*,*,#4922,.F.);
#6574=ORIENTED_EDGE('',*,*,#4924,.F.);
#6575=ORIENTED_EDGE('',*,*,#4921,.F.);
#6576=ORIENTED_EDGE('',*,*,#4918,.F.);
#6577=ORIENTED_EDGE('',*,*,#4915,.F.);
#6578=ORIENTED_EDGE('',*,*,#4912,.F.);
#6579=ORIENTED_EDGE('',*,*,#4908,.F.);
#6580=ORIENTED_EDGE('',*,*,#4925,.F.);
#6581=ORIENTED_EDGE('',*,*,#4910,.F.);
#6582=ORIENTED_EDGE('',*,*,#4914,.F.);
#6583=ORIENTED_EDGE('',*,*,#4917,.F.);
#6584=ORIENTED_EDGE('',*,*,#4920,.F.);
#6585=ORIENTED_EDGE('',*,*,#4923,.F.);
#6586=ORIENTED_EDGE('',*,*,#4926,.T.);
#6587=ORIENTED_EDGE('',*,*,#4927,.F.);
#6588=ORIENTED_EDGE('',*,*,#4926,.F.);
#6589=ORIENTED_EDGE('',*,*,#4928,.T.);
#6590=ORIENTED_EDGE('',*,*,#4929,.T.);
#6591=ORIENTED_EDGE('',*,*,#4928,.F.);
#6592=ORIENTED_EDGE('',*,*,#4929,.F.);
#6593=ORIENTED_EDGE('',*,*,#4930,.F.);
#6594=ORIENTED_EDGE('',*,*,#4931,.F.);
#6595=ORIENTED_EDGE('',*,*,#4932,.T.);
#6596=ORIENTED_EDGE('',*,*,#4930,.T.);
#6597=ORIENTED_EDGE('',*,*,#4932,.F.);
#6598=ORIENTED_EDGE('',*,*,#4933,.F.);
#6599=ORIENTED_EDGE('',*,*,#4934,.T.);
#6600=ORIENTED_EDGE('',*,*,#4931,.T.);
#6601=ORIENTED_EDGE('',*,*,#4934,.F.);
#6602=ORIENTED_EDGE('',*,*,#4935,.F.);
#6603=ORIENTED_EDGE('',*,*,#4936,.T.);
#6604=ORIENTED_EDGE('',*,*,#4933,.T.);
#6605=ORIENTED_EDGE('',*,*,#4936,.F.);
#6606=ORIENTED_EDGE('',*,*,#4935,.T.);
#6607=ORIENTED_EDGE('',*,*,#4937,.F.);
#6608=ORIENTED_EDGE('',*,*,#4938,.F.);
#6609=ORIENTED_EDGE('',*,*,#4939,.T.);
#6610=ORIENTED_EDGE('',*,*,#4937,.T.);
#6611=ORIENTED_EDGE('',*,*,#4939,.F.);
#6612=ORIENTED_EDGE('',*,*,#4927,.T.);
#6613=ORIENTED_EDGE('',*,*,#4940,.T.);
#6614=ORIENTED_EDGE('',*,*,#4938,.T.);
#6615=ORIENTED_EDGE('',*,*,#4940,.F.);
#7160=CYLINDRICAL_SURFACE('',#8434,0.25);
#7161=CYLINDRICAL_SURFACE('',#8441,0.425);
#7162=CYLINDRICAL_SURFACE('',#8449,0.24505);
#7475=ADVANCED_FACE('',(#1207),#824,.F.);
#7476=ADVANCED_FACE('',(#1208),#825,.F.);
#7477=ADVANCED_FACE('',(#1209),#826,.F.);
#7478=ADVANCED_FACE('',(#1210),#827,.F.);
#7479=ADVANCED_FACE('',(#1211),#828,.F.);
#7480=ADVANCED_FACE('',(#1212),#829,.F.);
#7481=ADVANCED_FACE('',(#1213),#830,.F.);
#7482=ADVANCED_FACE('',(#1214),#831,.F.);
#7483=ADVANCED_FACE('',(#1215,#568),#832,.T.);
#7484=ADVANCED_FACE('',(#1216),#7160,.T.);
#7485=ADVANCED_FACE('',(#1217),#833,.F.);
#7486=ADVANCED_FACE('',(#1218),#834,.T.);
#7487=ADVANCED_FACE('',(#1219),#336,.T.);
#7488=ADVANCED_FACE('',(#1220),#7161,.T.);
#7489=ADVANCED_FACE('',(#1221),#337,.T.);
#7490=ADVANCED_FACE('',(#1222,#569),#835,.T.);
#7491=ADVANCED_FACE('',(#1223),#338,.T.);
#7492=ADVANCED_FACE('',(#1224),#7162,.T.);
#7622=CLOSED_SHELL('',(#7475,#7476,#7477,#7478,#7479,#7480,#7481,#7482));
#7623=CLOSED_SHELL('',(#7483,#7484,#7485,#7486,#7487,#7488,#7489,#7490,
#7491,#7492));
#8422=AXIS2_PLACEMENT_3D('',#12353,#10135,#10136);
#8423=AXIS2_PLACEMENT_3D('',#12354,#10137,#10138);
#8424=AXIS2_PLACEMENT_3D('',#12363,#10143,#10144);
#8425=AXIS2_PLACEMENT_3D('',#12369,#10148,#10149);
#8426=AXIS2_PLACEMENT_3D('',#12375,#10153,#10154);
#8427=AXIS2_PLACEMENT_3D('',#12381,#10158,#10159);
#8428=AXIS2_PLACEMENT_3D('',#12387,#10163,#10164);
#8429=AXIS2_PLACEMENT_3D('',#12390,#10167,#10168);
#8430=AXIS2_PLACEMENT_3D('',#12391,#10169,#10170);
#8431=AXIS2_PLACEMENT_3D('',#12392,#10171,#10172);
#8432=AXIS2_PLACEMENT_3D('',#12394,#10173,#10174);
#8433=AXIS2_PLACEMENT_3D('',#12396,#10175,#10176);
#8434=AXIS2_PLACEMENT_3D('',#12397,#10177,#10178);
#8435=AXIS2_PLACEMENT_3D('',#12400,#10180,#10181);
#8436=AXIS2_PLACEMENT_3D('',#12401,#10182,#10183);
#8437=AXIS2_PLACEMENT_3D('',#12402,#10184,#10185);
#8438=AXIS2_PLACEMENT_3D('',#12404,#10186,#10187);
#8439=AXIS2_PLACEMENT_3D('',#12405,#10188,#10189);
#8440=AXIS2_PLACEMENT_3D('',#12407,#10190,#10191);
#8441=AXIS2_PLACEMENT_3D('',#12409,#10193,#10194);
#8442=AXIS2_PLACEMENT_3D('',#12411,#10195,#10196);
#8443=AXIS2_PLACEMENT_3D('',#12413,#10198,#10199);
#8444=AXIS2_PLACEMENT_3D('',#12415,#10200,#10201);
#8445=AXIS2_PLACEMENT_3D('',#12417,#10203,#10204);
#8446=AXIS2_PLACEMENT_3D('',#12419,#10205,#10206);
#8447=AXIS2_PLACEMENT_3D('',#12420,#10207,#10208);
#8448=AXIS2_PLACEMENT_3D('',#12422,#10209,#10210);
#8449=AXIS2_PLACEMENT_3D('',#12424,#10212,#10213);
#10135=DIRECTION('axis',(0.,0.,1.));
#10136=DIRECTION('refdir',(1.,0.,0.));
#10137=DIRECTION('center_axis',(0.866025403784439,0.,-0.5));
#10138=DIRECTION('ref_axis',(0.5,0.,0.866025403784439));
#10139=DIRECTION('',(-0.5,0.,-0.866025403784439));
#10140=DIRECTION('',(0.,-1.,0.));
#10141=DIRECTION('',(0.5,0.,0.866025403784439));
#10142=DIRECTION('',(0.,-1.,0.));
#10143=DIRECTION('center_axis',(1.20185167898973E-16,0.,-1.));
#10144=DIRECTION('ref_axis',(1.,0.,1.20185167898973E-16));
#10145=DIRECTION('',(-1.,0.,-1.20185167898973E-16));
#10146=DIRECTION('',(0.,-1.,0.));
#10147=DIRECTION('',(1.,0.,1.20185167898973E-16));
#10148=DIRECTION('center_axis',(-0.866025403784439,0.,-0.5));
#10149=DIRECTION('ref_axis',(0.5,0.,-0.866025403784439));
#10150=DIRECTION('',(-0.5,0.,0.866025403784439));
#10151=DIRECTION('',(0.,-1.,0.));
#10152=DIRECTION('',(0.5,0.,-0.866025403784439));
#10153=DIRECTION('center_axis',(-0.866025403784439,0.,0.5));
#10154=DIRECTION('ref_axis',(-0.5,0.,-0.866025403784439));
#10155=DIRECTION('',(0.5,0.,0.866025403784439));
#10156=DIRECTION('',(0.,-1.,0.));
#10157=DIRECTION('',(-0.5,0.,-0.866025403784439));
#10158=DIRECTION('center_axis',(-2.40370335797945E-16,0.,1.));
#10159=DIRECTION('ref_axis',(-1.,0.,-2.40370335797945E-16));
#10160=DIRECTION('',(1.,0.,2.40370335797945E-16));
#10161=DIRECTION('',(0.,-1.,0.));
#10162=DIRECTION('',(-1.,0.,-2.40370335797945E-16));
#10163=DIRECTION('center_axis',(0.866025403784439,0.,0.5));
#10164=DIRECTION('ref_axis',(-0.5,0.,0.866025403784439));
#10165=DIRECTION('',(0.5,0.,-0.866025403784439));
#10166=DIRECTION('',(-0.5,0.,0.866025403784439));
#10167=DIRECTION('center_axis',(0.,1.,0.));
#10168=DIRECTION('ref_axis',(1.,0.,0.));
#10169=DIRECTION('center_axis',(0.,-1.,0.));
#10170=DIRECTION('ref_axis',(0.,0.,-1.));
#10171=DIRECTION('center_axis',(0.,1.,0.));
#10172=DIRECTION('ref_axis',(1.,0.,0.));
#10173=DIRECTION('center_axis',(0.,1.,0.));
#10174=DIRECTION('ref_axis',(1.,0.,0.));
#10175=DIRECTION('center_axis',(0.,1.,0.));
#10176=DIRECTION('ref_axis',(1.,0.,0.));
#10177=DIRECTION('center_axis',(0.,1.,0.));
#10178=DIRECTION('ref_axis',(1.,0.,0.));
#10179=DIRECTION('',(0.,-1.,0.));
#10180=DIRECTION('center_axis',(0.,1.,0.));
#10181=DIRECTION('ref_axis',(1.,0.,0.));
#10182=DIRECTION('center_axis',(0.,1.,0.));
#10183=DIRECTION('ref_axis',(1.,0.,0.));
#10184=DIRECTION('center_axis',(0.,1.,0.));
#10185=DIRECTION('ref_axis',(0.,0.,1.));
#10186=DIRECTION('center_axis',(0.,-1.,0.));
#10187=DIRECTION('ref_axis',(1.,0.,0.));
#10188=DIRECTION('center_axis',(0.,-1.,0.));
#10189=DIRECTION('ref_axis',(1.,0.,0.));
#10190=DIRECTION('center_axis',(0.,-1.,0.));
#10191=DIRECTION('ref_axis',(1.,0.,0.));
#10192=DIRECTION('',(0.707106781186548,0.707106781186547,8.65956056235493E-17));
#10193=DIRECTION('center_axis',(0.,-1.,0.));
#10194=DIRECTION('ref_axis',(1.,0.,0.));
#10195=DIRECTION('center_axis',(0.,-1.,0.));
#10196=DIRECTION('ref_axis',(1.,0.,0.));
#10197=DIRECTION('',(0.,1.,0.));
#10198=DIRECTION('center_axis',(0.,1.,0.));
#10199=DIRECTION('ref_axis',(1.,0.,0.));
#10200=DIRECTION('center_axis',(0.,-1.,0.));
#10201=DIRECTION('ref_axis',(1.,0.,0.));
#10202=DIRECTION('',(-0.707106781186547,0.707106781186548,-8.65956056235493E-17));
#10203=DIRECTION('center_axis',(0.,-1.,0.));
#10204=DIRECTION('ref_axis',(0.,0.,-1.));
#10205=DIRECTION('center_axis',(0.,-1.,0.));
#10206=DIRECTION('ref_axis',(1.,0.,0.));
#10207=DIRECTION('center_axis',(0.,1.,0.));
#10208=DIRECTION('ref_axis',(1.,0.,0.));
#10209=DIRECTION('center_axis',(0.,1.,0.));
#10210=DIRECTION('ref_axis',(1.,0.,0.));
#10211=DIRECTION('',(-0.447213595499958,0.894427190999916,-5.47678698264203E-17));
#10212=DIRECTION('center_axis',(0.,-1.,0.));
#10213=DIRECTION('ref_axis',(1.,0.,0.));
#10214=DIRECTION('',(0.,1.,0.));
#12353=CARTESIAN_POINT('',(0.,0.,0.));
#12354=CARTESIAN_POINT('Origin',(0.115470053837925,-0.5,-0.2));
#12355=CARTESIAN_POINT('',(0.23094010767585,-0.5,0.));
#12356=CARTESIAN_POINT('',(0.115470053837925,-0.5,-0.2));
#12357=CARTESIAN_POINT('',(0.23094010767585,-0.5,0.));
#12358=CARTESIAN_POINT('',(0.115470053837925,-0.8,-0.2));
#12359=CARTESIAN_POINT('',(0.115470053837925,-0.5,-0.2));
#12360=CARTESIAN_POINT('',(0.23094010767585,-0.8,0.));
#12361=CARTESIAN_POINT('',(0.23094010767585,-0.8,0.));
#12362=CARTESIAN_POINT('',(0.23094010767585,-0.5,0.));
#12363=CARTESIAN_POINT('Origin',(-0.115470053837925,-0.5,-0.2));
#12364=CARTESIAN_POINT('',(-0.115470053837925,-0.5,-0.2));
#12365=CARTESIAN_POINT('',(0.115470053837925,-0.5,-0.2));
#12366=CARTESIAN_POINT('',(-0.115470053837925,-0.8,-0.2));
#12367=CARTESIAN_POINT('',(-0.115470053837925,-0.5,-0.2));
#12368=CARTESIAN_POINT('',(0.115470053837925,-0.8,-0.2));
#12369=CARTESIAN_POINT('Origin',(-0.23094010767585,-0.5,-2.77555756156289E-17));
#12370=CARTESIAN_POINT('',(-0.23094010767585,-0.5,-2.82820063659975E-17));
#12371=CARTESIAN_POINT('',(-0.115470053837925,-0.5,-0.2));
#12372=CARTESIAN_POINT('',(-0.23094010767585,-0.8,-2.77555756156289E-17));
#12373=CARTESIAN_POINT('',(-0.23094010767585,-0.5,-2.82820063659975E-17));
#12374=CARTESIAN_POINT('',(-0.115470053837925,-0.8,-0.2));
#12375=CARTESIAN_POINT('Origin',(-0.115470053837925,-0.5,0.2));
#12376=CARTESIAN_POINT('',(-0.115470053837925,-0.5,0.2));
#12377=CARTESIAN_POINT('',(-0.23094010767585,-0.5,-2.82820063659975E-17));
#12378=CARTESIAN_POINT('',(-0.115470053837925,-0.8,0.2));
#12379=CARTESIAN_POINT('',(-0.115470053837925,-0.5,0.2));
#12380=CARTESIAN_POINT('',(-0.23094010767585,-0.8,-2.82820063659975E-17));
#12381=CARTESIAN_POINT('Origin',(0.115470053837925,-0.5,0.2));
#12382=CARTESIAN_POINT('',(0.115470053837925,-0.5,0.2));
#12383=CARTESIAN_POINT('',(-0.115470053837925,-0.5,0.2));
#12384=CARTESIAN_POINT('',(0.115470053837925,-0.8,0.2));
#12385=CARTESIAN_POINT('',(0.115470053837925,-0.5,0.2));
#12386=CARTESIAN_POINT('',(-0.115470053837925,-0.8,0.2));
#12387=CARTESIAN_POINT('Origin',(0.23094010767585,-0.5,0.));
#12388=CARTESIAN_POINT('',(0.115470053837925,-0.5,0.2));
#12389=CARTESIAN_POINT('',(0.115470053837925,-0.8,0.2));
#12390=CARTESIAN_POINT('Origin',(0.,-0.5,0.));
#12391=CARTESIAN_POINT('Origin',(0.,-0.8,0.));
#12392=CARTESIAN_POINT('Origin',(0.,-1.9,0.));
#12393=CARTESIAN_POINT('',(-0.25,-1.9,3.06161699786838E-17));
#12394=CARTESIAN_POINT('Origin',(0.,-1.9,0.));
#12395=CARTESIAN_POINT('',(-0.24505,-1.9,3.00099698131059E-17));
#12396=CARTESIAN_POINT('Origin',(0.,-1.9,0.));
#12397=CARTESIAN_POINT('Origin',(0.,-3.,0.));
#12398=CARTESIAN_POINT('',(-0.25,-3.,3.06161699786838E-17));
#12399=CARTESIAN_POINT('',(-0.25,-3.,3.06161699786838E-17));
#12400=CARTESIAN_POINT('Origin',(0.,-3.,0.));
#12401=CARTESIAN_POINT('Origin',(0.,-3.,0.));
#12402=CARTESIAN_POINT('Origin',(0.375,0.5,0.));
#12403=CARTESIAN_POINT('',(-0.375,0.5,-4.59242549680257E-17));
#12404=CARTESIAN_POINT('Origin',(0.,0.5,0.));
#12405=CARTESIAN_POINT('Origin',(0.,0.475,0.));
#12406=CARTESIAN_POINT('',(-0.425,0.45,-5.20474889637625E-17));
#12407=CARTESIAN_POINT('Origin',(0.,0.45,0.));
#12408=CARTESIAN_POINT('',(-0.4,0.475,-4.89858719658941E-17));
#12409=CARTESIAN_POINT('Origin',(0.,0.24,0.));
#12410=CARTESIAN_POINT('',(-0.425,0.0299999999999998,-5.20474889637625E-17));
#12411=CARTESIAN_POINT('Origin',(0.,0.0299999999999998,0.));
#12412=CARTESIAN_POINT('',(-0.425,0.24,-5.20474889637625E-17));
#12413=CARTESIAN_POINT('Origin',(0.,0.0150000000000001,0.));
#12414=CARTESIAN_POINT('',(-0.395,4.85722573273506E-17,-4.83735485663204E-17));
#12415=CARTESIAN_POINT('Origin',(0.,0.,0.));
#12416=CARTESIAN_POINT('',(-0.41,0.0150000000000001,-5.02105187650415E-17));
#12417=CARTESIAN_POINT('Origin',(0.27,0.,0.));
#12418=CARTESIAN_POINT('',(-0.27,0.,-3.30654635769785E-17));
#12419=CARTESIAN_POINT('Origin',(0.,0.,0.));
#12420=CARTESIAN_POINT('Origin',(0.,-0.02,0.));
#12421=CARTESIAN_POINT('',(-0.24505,-0.0498999999999999,3.00099698131059E-17));
#12422=CARTESIAN_POINT('Origin',(0.,-0.0498999999999999,0.));
#12423=CARTESIAN_POINT('',(-0.26,-0.02,-3.18408167778312E-17));
#12424=CARTESIAN_POINT('Origin',(0.,-0.995,0.));
#12425=CARTESIAN_POINT('',(-0.24505,-0.995,-3.00099698131059E-17));
#13047=UNCERTAINTY_MEASURE_WITH_UNIT(LENGTH_MEASURE(0.001),#13095,
'DISTANCE_ACCURACY_VALUE',
'Maximum model space distance between geometric entities at asserted c
onnectivities');
#13057=UNCERTAINTY_MEASURE_WITH_UNIT(LENGTH_MEASURE(0.001),#13095,
'DISTANCE_ACCURACY_VALUE',
'Maximum model space distance between geometric entities at asserted c
onnectivities');
#13084=(
GEOMETRIC_REPRESENTATION_CONTEXT(3)
GLOBAL_UNCERTAINTY_ASSIGNED_CONTEXT((#13047))
GLOBAL_UNIT_ASSIGNED_CONTEXT((#13095,#13097,#13098))
REPRESENTATION_CONTEXT('','3D')
);
#13094=(
GEOMETRIC_REPRESENTATION_CONTEXT(3)
GLOBAL_UNCERTAINTY_ASSIGNED_CONTEXT((#13057))
GLOBAL_UNIT_ASSIGNED_CONTEXT((#13095,#13097,#13098))
REPRESENTATION_CONTEXT('','3D')
);
#13095=(
LENGTH_UNIT()
NAMED_UNIT(*)
SI_UNIT(.CENTI.,.METRE.)
);
#13097=(
NAMED_UNIT(*)
PLANE_ANGLE_UNIT()
SI_UNIT($,.RADIAN.)
);
#13098=(
NAMED_UNIT(*)
SI_UNIT($,.STERADIAN.)
SOLID_ANGLE_UNIT()
);
#13125=SHAPE_DEFINITION_REPRESENTATION(#13161,#13275);
#13161=PRODUCT_DEFINITION_SHAPE('',$,#13312);
#13275=SHAPE_REPRESENTATION('',(#8422),#13084);
#13285=PRODUCT_DEFINITION_CONTEXT('part definition',#13395,'design');
#13312=PRODUCT_DEFINITION('M5x30 frame screw','M5x30 frame screw',#13348,
#13285);
#13348=PRODUCT_DEFINITION_FORMATION('',$,#13423);
#13395=APPLICATION_CONTEXT(
'Core Data for Automotive Mechanical Design Process');
#13396=PRODUCT_CONTEXT('part definition',#13395,'mechanical');
#13423=PRODUCT('M5x30 frame screw','M5x30 frame screw',
'M5x30 frame screw',(#13396));
#13496=COLOUR_RGB('Black',0.12,0.14,0.17);
#13497=FILL_AREA_STYLE_COLOUR('',#13496);
#13498=FILL_AREA_STYLE('',(#13497));
#13499=SURFACE_STYLE_FILL_AREA(#13498);
#13500=SURFACE_SIDE_STYLE('',(#13499));
#13501=SURFACE_STYLE_USAGE(.BOTH.,#13500);
#13502=PRESENTATION_STYLE_ASSIGNMENT((#13501));
ENDSEC;
END-ISO-10303-21;
